ISO-10303-21;
HEADER;
/* Generated by software containing ST-Developer
 * from STEP Tools, Inc. (www.steptools.com) 
 */

FILE_DESCRIPTION(
/* description */ ('PAT-023'),
/* implementation_level */ '2;1');

FILE_NAME(
/* name */ 'Hex Bolt - M6 x 30 mm.step',
/* time_stamp */ '2026-10-29T15:47:46-07:00',
/* author */ (''),
/* organization */ (''),
/* preprocessor_version */ 'ST-DEVELOPER v20.2',
/* originating_system */ 'Autodesk Translation Framework v15.17.0.0',
/* authorisation */ '');

FILE_SCHEMA (('AUTOMOTIVE_DESIGN { 1 0 10303 214 3 1 1 }'));
ENDSEC;

DATA;
#10=MECHANICAL_DESIGN_GEOMETRIC_PRESENTATION_REPRESENTATION('',(#90),#3773);
#11=(
BOUNDED_CURVE()
B_SPLINE_CURVE(2,(#3418,#3419,#3420),.UNSPECIFIED.,.F.,.F.)
B_SPLINE_CURVE_WITH_KNOTS((3,3),(0.144988513094728,0.791574906712449),
 .UNSPECIFIED.)
CURVE()
GEOMETRIC_REPRESENTATION_ITEM()
RATIONAL_B_SPLINE_CURVE((1.09282032302755,1.26188021535082,1.09282032302931))
REPRESENTATION_ITEM('')
);
#12=(
BOUNDED_CURVE()
B_SPLINE_CURVE(2,(#3422,#3423,#3424),.UNSPECIFIED.,.F.,.F.)
B_SPLINE_CURVE_WITH_KNOTS((3,3),(0.144988513094728,0.791574906712449),
 .UNSPECIFIED.)
CURVE()
GEOMETRIC_REPRESENTATION_ITEM()
RATIONAL_B_SPLINE_CURVE((1.09282032302755,1.26188021535082,1.09282032302931))
REPRESENTATION_ITEM('')
);
#13=(
BOUNDED_CURVE()
B_SPLINE_CURVE(2,(#3426,#3427,#3428),.UNSPECIFIED.,.F.,.F.)
B_SPLINE_CURVE_WITH_KNOTS((3,3),(0.144988513094728,0.791574906712449),
 .UNSPECIFIED.)
CURVE()
GEOMETRIC_REPRESENTATION_ITEM()
RATIONAL_B_SPLINE_CURVE((1.09282032302755,1.26188021535082,1.09282032302931))
REPRESENTATION_ITEM('')
);
#14=(
BOUNDED_CURVE()
B_SPLINE_CURVE(2,(#3430,#3431,#3432),.UNSPECIFIED.,.F.,.F.)
B_SPLINE_CURVE_WITH_KNOTS((3,3),(0.144988513094728,0.791574906712449),
 .UNSPECIFIED.)
CURVE()
GEOMETRIC_REPRESENTATION_ITEM()
RATIONAL_B_SPLINE_CURVE((1.09282032302755,1.26188021535082,1.09282032302931))
REPRESENTATION_ITEM('')
);
#15=(
BOUNDED_CURVE()
B_SPLINE_CURVE(2,(#3434,#3435,#3436),.UNSPECIFIED.,.F.,.F.)
B_SPLINE_CURVE_WITH_KNOTS((3,3),(0.144988513094728,0.791574906712449),
 .UNSPECIFIED.)
CURVE()
GEOMETRIC_REPRESENTATION_ITEM()
RATIONAL_B_SPLINE_CURVE((1.09282032302755,1.26188021535082,1.09282032302931))
REPRESENTATION_ITEM('')
);
#16=(
BOUNDED_CURVE()
B_SPLINE_CURVE(2,(#3437,#3438,#3439),.UNSPECIFIED.,.F.,.F.)
B_SPLINE_CURVE_WITH_KNOTS((3,3),(0.144988513094727,0.791574906712449),
 .UNSPECIFIED.)
CURVE()
GEOMETRIC_REPRESENTATION_ITEM()
RATIONAL_B_SPLINE_CURVE((1.09282032302755,1.26188021535082,1.09282032302931))
REPRESENTATION_ITEM('')
);
#66=CONICAL_SURFACE('',#2430,0.27,0.785398163397448);
#67=CONICAL_SURFACE('',#2433,0.576175134594813,1.0471975511966);
#74=SHAPE_REPRESENTATION_RELATIONSHIP('SRR','None',#3822,#82);
#82=ADVANCED_BREP_SHAPE_REPRESENTATION('',(#98),#3770);
#90=STYLED_ITEM('',(#3953),#98);
#98=MANIFOLD_SOLID_BREP('Body1',#2243);
#112=FACE_BOUND('',#421,.T.);
#163=PLANE('',#2432);
#164=PLANE('',#2435);
#165=PLANE('',#2436);
#166=PLANE('',#2437);
#167=PLANE('',#2438);
#168=PLANE('',#2439);
#169=PLANE('',#2440);
#170=PLANE('',#2441);
#171=PLANE('',#2442);
#278=FACE_OUTER_BOUND('',#409,.T.);
#279=FACE_OUTER_BOUND('',#410,.T.);
#280=FACE_OUTER_BOUND('',#411,.T.);
#281=FACE_OUTER_BOUND('',#412,.T.);
#282=FACE_OUTER_BOUND('',#413,.T.);
#283=FACE_OUTER_BOUND('',#414,.T.);
#284=FACE_OUTER_BOUND('',#415,.T.);
#285=FACE_OUTER_BOUND('',#416,.T.);
#286=FACE_OUTER_BOUND('',#417,.T.);
#287=FACE_OUTER_BOUND('',#418,.T.);
#288=FACE_OUTER_BOUND('',#419,.T.);
#289=FACE_OUTER_BOUND('',#420,.T.);
#409=EDGE_LOOP('',(#1789,#1790,#1791,#1792));
#410=EDGE_LOOP('',(#1793,#1794,#1795,#1796));
#411=EDGE_LOOP('',(#1797));
#412=EDGE_LOOP('',(#1798,#1799,#1800,#1801,#1802,#1803,#1804,#1805,#1806));
#413=EDGE_LOOP('',(#1807,#1808,#1809,#1810));
#414=EDGE_LOOP('',(#1811,#1812,#1813,#1814));
#415=EDGE_LOOP('',(#1815,#1816,#1817,#1818));
#416=EDGE_LOOP('',(#1819,#1820,#1821,#1822));
#417=EDGE_LOOP('',(#1823,#1824,#1825,#1826));
#418=EDGE_LOOP('',(#1827,#1828,#1829,#1830));
#419=EDGE_LOOP('',(#1831));
#420=EDGE_LOOP('',(#1832,#1833,#1834,#1835,#1836,#1837));
#421=EDGE_LOOP('',(#1838));
#587=LINE('',#3405,#851);
#588=LINE('',#3410,#852);
#589=LINE('',#3416,#853);
#590=LINE('',#3442,#854);
#591=LINE('',#3444,#855);
#592=LINE('',#3445,#856);
#593=LINE('',#3448,#857);
#594=LINE('',#3449,#858);
#595=LINE('',#3452,#859);
#596=LINE('',#3453,#860);
#597=LINE('',#3456,#861);
#598=LINE('',#3457,#862);
#599=LINE('',#3460,#863);
#600=LINE('',#3461,#864);
#601=LINE('',#3463,#865);
#851=VECTOR('',#2808,0.3);
#852=VECTOR('',#2815,0.27);
#853=VECTOR('',#2822,0.576175134594813);
#854=VECTOR('',#2825,1.);
#855=VECTOR('',#2826,1.);
#856=VECTOR('',#2827,1.);
#857=VECTOR('',#2830,1.);
#858=VECTOR('',#2831,1.);
#859=VECTOR('',#2834,1.);
#860=VECTOR('',#2835,1.);
#861=VECTOR('',#2838,1.);
#862=VECTOR('',#2839,1.);
#863=VECTOR('',#2842,1.);
#864=VECTOR('',#2843,1.);
#865=VECTOR('',#2846,1.);
#1019=CIRCLE('',#2428,0.2942);
#1020=CIRCLE('',#2429,0.2942);
#1021=CIRCLE('',#2431,0.24);
#1022=CIRCLE('',#2434,0.475);
#1115=VERTEX_POINT('',#3402);
#1116=VERTEX_POINT('',#3404);
#1117=VERTEX_POINT('',#3408);
#1118=VERTEX_POINT('',#3413);
#1119=VERTEX_POINT('',#3415);
#1120=VERTEX_POINT('',#3417);
#1121=VERTEX_POINT('',#3421);
#1122=VERTEX_POINT('',#3425);
#1123=VERTEX_POINT('',#3429);
#1124=VERTEX_POINT('',#3433);
#1125=VERTEX_POINT('',#3441);
#1126=VERTEX_POINT('',#3443);
#1127=VERTEX_POINT('',#3447);
#1128=VERTEX_POINT('',#3451);
#1129=VERTEX_POINT('',#3455);
#1130=VERTEX_POINT('',#3459);
#1357=EDGE_CURVE('',#1115,#1115,#1019,.F.);
#1358=EDGE_CURVE('',#1115,#1116,#587,.T.);
#1359=EDGE_CURVE('',#1116,#1116,#1020,.F.);
#1360=EDGE_CURVE('',#1117,#1117,#1021,.T.);
#1361=EDGE_CURVE('',#1117,#1115,#588,.T.);
#1362=EDGE_CURVE('',#1118,#1118,#1022,.T.);
#1363=EDGE_CURVE('',#1118,#1119,#589,.T.);
#1364=EDGE_CURVE('',#1120,#1119,#11,.T.);
#1365=EDGE_CURVE('',#1121,#1120,#12,.T.);
#1366=EDGE_CURVE('',#1122,#1121,#13,.T.);
#1367=EDGE_CURVE('',#1123,#1122,#14,.T.);
#1368=EDGE_CURVE('',#1124,#1123,#15,.T.);
#1369=EDGE_CURVE('',#1119,#1124,#16,.T.);
#1370=EDGE_CURVE('',#1125,#1123,#590,.T.);
#1371=EDGE_CURVE('',#1125,#1126,#591,.T.);
#1372=EDGE_CURVE('',#1126,#1124,#592,.T.);
#1373=EDGE_CURVE('',#1127,#1122,#593,.T.);
#1374=EDGE_CURVE('',#1127,#1125,#594,.T.);
#1375=EDGE_CURVE('',#1128,#1121,#595,.T.);
#1376=EDGE_CURVE('',#1128,#1127,#596,.T.);
#1377=EDGE_CURVE('',#1129,#1120,#597,.T.);
#1378=EDGE_CURVE('',#1129,#1128,#598,.T.);
#1379=EDGE_CURVE('',#1130,#1119,#599,.T.);
#1380=EDGE_CURVE('',#1130,#1129,#600,.T.);
#1381=EDGE_CURVE('',#1126,#1130,#601,.T.);
#1789=ORIENTED_EDGE('',*,*,#1357,.F.);
#1790=ORIENTED_EDGE('',*,*,#1358,.T.);
#1791=ORIENTED_EDGE('',*,*,#1359,.F.);
#1792=ORIENTED_EDGE('',*,*,#1358,.F.);
#1793=ORIENTED_EDGE('',*,*,#1360,.F.);
#1794=ORIENTED_EDGE('',*,*,#1361,.T.);
#1795=ORIENTED_EDGE('',*,*,#1357,.T.);
#1796=ORIENTED_EDGE('',*,*,#1361,.F.);
#1797=ORIENTED_EDGE('',*,*,#1360,.T.);
#1798=ORIENTED_EDGE('',*,*,#1362,.F.);
#1799=ORIENTED_EDGE('',*,*,#1363,.T.);
#1800=ORIENTED_EDGE('',*,*,#1364,.F.);
#1801=ORIENTED_EDGE('',*,*,#1365,.F.);
#1802=ORIENTED_EDGE('',*,*,#1366,.F.);
#1803=ORIENTED_EDGE('',*,*,#1367,.F.);
#1804=ORIENTED_EDGE('',*,*,#1368,.F.);
#1805=ORIENTED_EDGE('',*,*,#1369,.F.);
#1806=ORIENTED_EDGE('',*,*,#1363,.F.);
#1807=ORIENTED_EDGE('',*,*,#1368,.T.);
#1808=ORIENTED_EDGE('',*,*,#1370,.F.);
#1809=ORIENTED_EDGE('',*,*,#1371,.T.);
#1810=ORIENTED_EDGE('',*,*,#1372,.T.);
#1811=ORIENTED_EDGE('',*,*,#1367,.T.);
#1812=ORIENTED_EDGE('',*,*,#1373,.F.);
#1813=ORIENTED_EDGE('',*,*,#1374,.T.);
#1814=ORIENTED_EDGE('',*,*,#1370,.T.);
#1815=ORIENTED_EDGE('',*,*,#1366,.T.);
#1816=ORIENTED_EDGE('',*,*,#1375,.F.);
#1817=ORIENTED_EDGE('',*,*,#1376,.T.);
#1818=ORIENTED_EDGE('',*,*,#1373,.T.);
#1819=ORIENTED_EDGE('',*,*,#1365,.T.);
#1820=ORIENTED_EDGE('',*,*,#1377,.F.);
#1821=ORIENTED_EDGE('',*,*,#1378,.T.);
#1822=ORIENTED_EDGE('',*,*,#1375,.T.);
#1823=ORIENTED_EDGE('',*,*,#1364,.T.);
#1824=ORIENTED_EDGE('',*,*,#1379,.F.);
#1825=ORIENTED_EDGE('',*,*,#1380,.T.);
#1826=ORIENTED_EDGE('',*,*,#1377,.T.);
#1827=ORIENTED_EDGE('',*,*,#1369,.T.);
#1828=ORIENTED_EDGE('',*,*,#1372,.F.);
#1829=ORIENTED_EDGE('',*,*,#1381,.T.);
#1830=ORIENTED_EDGE('',*,*,#1379,.T.);
#1831=ORIENTED_EDGE('',*,*,#1362,.T.);
#1832=ORIENTED_EDGE('',*,*,#1376,.F.);
#1833=ORIENTED_EDGE('',*,*,#1378,.F.);
#1834=ORIENTED_EDGE('',*,*,#1380,.F.);
#1835=ORIENTED_EDGE('',*,*,#1381,.F.);
#1836=ORIENTED_EDGE('',*,*,#1371,.F.);
#1837=ORIENTED_EDGE('',*,*,#1374,.F.);
#1838=ORIENTED_EDGE('',*,*,#1359,.T.);
#2116=CYLINDRICAL_SURFACE('',#2427,0.2942);
#2178=ADVANCED_FACE('',(#278),#2116,.T.);
#2179=ADVANCED_FACE('',(#279),#66,.T.);
#2180=ADVANCED_FACE('',(#280),#163,.T.);
#2181=ADVANCED_FACE('',(#281),#67,.T.);
#2182=ADVANCED_FACE('',(#282),#164,.T.);
#2183=ADVANCED_FACE('',(#283),#165,.T.);
#2184=ADVANCED_FACE('',(#284),#166,.T.);
#2185=ADVANCED_FACE('',(#285),#167,.T.);
#2186=ADVANCED_FACE('',(#286),#168,.T.);
#2187=ADVANCED_FACE('',(#287),#169,.T.);
#2188=ADVANCED_FACE('',(#288),#170,.T.);
#2189=ADVANCED_FACE('',(#289,#112),#171,.F.);
#2243=CLOSED_SHELL('',(#2178,#2179,#2180,#2181,#2182,#2183,#2184,#2185,
#2186,#2187,#2188,#2189));
#2426=AXIS2_PLACEMENT_3D('',#3400,#2802,#2803);
#2427=AXIS2_PLACEMENT_3D('',#3401,#2804,#2805);
#2428=AXIS2_PLACEMENT_3D('',#3403,#2806,#2807);
#2429=AXIS2_PLACEMENT_3D('',#3406,#2809,#2810);
#2430=AXIS2_PLACEMENT_3D('',#3407,#2811,#2812);
#2431=AXIS2_PLACEMENT_3D('',#3409,#2813,#2814);
#2432=AXIS2_PLACEMENT_3D('',#3411,#2816,#2817);
#2433=AXIS2_PLACEMENT_3D('',#3412,#2818,#2819);
#2434=AXIS2_PLACEMENT_3D('',#3414,#2820,#2821);
#2435=AXIS2_PLACEMENT_3D('',#3440,#2823,#2824);
#2436=AXIS2_PLACEMENT_3D('',#3446,#2828,#2829);
#2437=AXIS2_PLACEMENT_3D('',#3450,#2832,#2833);
#2438=AXIS2_PLACEMENT_3D('',#3454,#2836,#2837);
#2439=AXIS2_PLACEMENT_3D('',#3458,#2840,#2841);
#2440=AXIS2_PLACEMENT_3D('',#3462,#2844,#2845);
#2441=AXIS2_PLACEMENT_3D('',#3464,#2847,#2848);
#2442=AXIS2_PLACEMENT_3D('',#3465,#2849,#2850);
#2802=DIRECTION('axis',(0.,0.,1.));
#2803=DIRECTION('refdir',(1.,0.,0.));
#2804=DIRECTION('center_axis',(0.,-1.,0.));
#2805=DIRECTION('ref_axis',(1.,0.,0.));
#2806=DIRECTION('center_axis',(0.,1.,0.));
#2807=DIRECTION('ref_axis',(1.,0.,0.));
#2808=DIRECTION('',(0.,1.,0.));
#2809=DIRECTION('center_axis',(0.,-1.,0.));
#2810=DIRECTION('ref_axis',(1.,0.,0.));
#2811=DIRECTION('center_axis',(0.,1.,0.));
#2812=DIRECTION('ref_axis',(1.,0.,0.));
#2813=DIRECTION('center_axis',(0.,-1.,0.));
#2814=DIRECTION('ref_axis',(1.,0.,0.));
#2815=DIRECTION('',(-0.707106781186547,0.707106781186548,-8.65956056235493E-17));
#2816=DIRECTION('center_axis',(0.,-1.,0.));
#2817=DIRECTION('ref_axis',(0.,0.,-1.));
#2818=DIRECTION('center_axis',(0.,-1.,0.));
#2819=DIRECTION('ref_axis',(1.,0.,0.));
#2820=DIRECTION('center_axis',(0.,1.,0.));
#2821=DIRECTION('ref_axis',(1.,0.,0.));
#2822=DIRECTION('',(-0.866025403784439,-0.5,-1.06057523872491E-16));
#2823=DIRECTION('center_axis',(1.92296268638356E-16,0.,-1.));
#2824=DIRECTION('ref_axis',(-1.,0.,-1.92296268638356E-16));
#2825=DIRECTION('',(0.,1.,0.));
#2826=DIRECTION('',(-1.,0.,-1.92296268638356E-16));
#2827=DIRECTION('',(0.,1.,0.));
#2828=DIRECTION('center_axis',(0.866025403784439,0.,-0.5));
#2829=DIRECTION('ref_axis',(-0.5,0.,-0.866025403784439));
#2830=DIRECTION('',(0.,1.,0.));
#2831=DIRECTION('',(-0.5,0.,-0.866025403784439));
#2832=DIRECTION('center_axis',(0.866025403784439,0.,0.5));
#2833=DIRECTION('ref_axis',(0.5,0.,-0.866025403784439));
#2834=DIRECTION('',(0.,1.,0.));
#2835=DIRECTION('',(0.5,0.,-0.866025403784439));
#2836=DIRECTION('center_axis',(-1.92296268638356E-16,0.,1.));
#2837=DIRECTION('ref_axis',(1.,0.,1.92296268638356E-16));
#2838=DIRECTION('',(0.,1.,0.));
#2839=DIRECTION('',(1.,0.,1.92296268638356E-16));
#2840=DIRECTION('center_axis',(-0.866025403784439,0.,0.5));
#2841=DIRECTION('ref_axis',(0.5,0.,0.866025403784439));
#2842=DIRECTION('',(0.,1.,0.));
#2843=DIRECTION('',(0.5,0.,0.866025403784439));
#2844=DIRECTION('center_axis',(-0.866025403784439,0.,-0.5));
#2845=DIRECTION('ref_axis',(-0.5,0.,0.866025403784439));
#2846=DIRECTION('',(-0.5,0.,0.866025403784438));
#2847=DIRECTION('center_axis',(0.,1.,0.));
#2848=DIRECTION('ref_axis',(0.,0.,1.));
#2849=DIRECTION('center_axis',(0.,1.,0.));
#2850=DIRECTION('ref_axis',(1.,0.,0.));
#3400=CARTESIAN_POINT('',(0.,0.,0.));
#3401=CARTESIAN_POINT('Origin',(0.,-1.445,0.));
#3402=CARTESIAN_POINT('',(-0.2942,-2.9458,3.60291088309151E-17));
#3403=CARTESIAN_POINT('Origin',(0.,-2.9458,0.));
#3404=CARTESIAN_POINT('',(-0.2942,0.,-3.60291088309151E-17));
#3405=CARTESIAN_POINT('',(-0.2942,-1.445,-3.60291088309151E-17));
#3406=CARTESIAN_POINT('Origin',(0.,0.,0.));
#3407=CARTESIAN_POINT('Origin',(0.,-2.97,0.));
#3408=CARTESIAN_POINT('',(-0.24,-3.,-2.93915231795365E-17));
#3409=CARTESIAN_POINT('Origin',(0.,-3.,0.));
#3410=CARTESIAN_POINT('',(-0.27,-2.97,-3.30654635769785E-17));
#3411=CARTESIAN_POINT('Origin',(0.,-3.,0.));
#3412=CARTESIAN_POINT('Origin',(0.,0.341586508806388,0.));
#3413=CARTESIAN_POINT('',(-0.475,0.4,-5.81707229594993E-17));
#3414=CARTESIAN_POINT('Origin',(0.,0.4,0.));
#3415=CARTESIAN_POINT('',(-0.577350269189626,0.340908044531739,-7.07050159149938E-17));
#3416=CARTESIAN_POINT('',(-0.576175134594813,0.341586508806388,-7.05611034329833E-17));
#3417=CARTESIAN_POINT('',(-0.288675134594813,0.340908044531739,0.5));
#3418=CARTESIAN_POINT('Ctrl Pts',(-0.288675134594813,0.340908044531739,
0.5));
#3419=CARTESIAN_POINT('Ctrl Pts',(-0.433012701893303,0.424241377863696,
0.249999999998124));
#3420=CARTESIAN_POINT('Ctrl Pts',(-0.577350269189626,0.340908044531739,
-7.07050159149938E-17));
#3421=CARTESIAN_POINT('',(0.288675134594813,0.340908044531739,0.5));
#3422=CARTESIAN_POINT('Ctrl Pts',(0.288675134594813,0.340908044531739,0.5));
#3423=CARTESIAN_POINT('Ctrl Pts',(-2.16648921025353E-12,0.424241377863696,
0.5));
#3424=CARTESIAN_POINT('Ctrl Pts',(-0.288675134594813,0.340908044531739,
0.5));
#3425=CARTESIAN_POINT('',(0.577350269189626,0.340908044531739,0.));
#3426=CARTESIAN_POINT('Ctrl Pts',(0.577350269189626,0.340908044531739,0.));
#3427=CARTESIAN_POINT('Ctrl Pts',(0.433012701891136,0.424241377863697,0.250000000001876));
#3428=CARTESIAN_POINT('Ctrl Pts',(0.288675134594813,0.340908044531739,0.5));
#3429=CARTESIAN_POINT('',(0.288675134594813,0.340908044531739,-0.5));
#3430=CARTESIAN_POINT('Ctrl Pts',(0.288675134594813,0.340908044531739,-0.5));
#3431=CARTESIAN_POINT('Ctrl Pts',(0.433012701893303,0.424241377863696,-0.249999999998124));
#3432=CARTESIAN_POINT('Ctrl Pts',(0.577350269189626,0.340908044531739,0.));
#3433=CARTESIAN_POINT('',(-0.288675134594813,0.340908044531739,-0.5));
#3434=CARTESIAN_POINT('Ctrl Pts',(-0.288675134594813,0.340908044531739,
-0.5));
#3435=CARTESIAN_POINT('Ctrl Pts',(2.16660023255599E-12,0.424241377863696,
-0.5));
#3436=CARTESIAN_POINT('Ctrl Pts',(0.288675134594813,0.340908044531739,-0.5));
#3437=CARTESIAN_POINT('Ctrl Pts',(-0.577350269189626,0.340908044531739,
-7.07050159149938E-17));
#3438=CARTESIAN_POINT('Ctrl Pts',(-0.433012701891136,0.424241377863697,
-0.250000000001876));
#3439=CARTESIAN_POINT('Ctrl Pts',(-0.288675134594813,0.340908044531739,
-0.5));
#3440=CARTESIAN_POINT('Origin',(0.288675134594813,0.,-0.5));
#3441=CARTESIAN_POINT('',(0.288675134594813,0.,-0.5));
#3442=CARTESIAN_POINT('',(0.288675134594813,0.,-0.5));
#3443=CARTESIAN_POINT('',(-0.288675134594813,0.,-0.5));
#3444=CARTESIAN_POINT('',(0.288675134594813,0.,-0.5));
#3445=CARTESIAN_POINT('',(-0.288675134594813,0.,-0.5));
#3446=CARTESIAN_POINT('Origin',(0.577350269189626,0.,0.));
#3447=CARTESIAN_POINT('',(0.577350269189626,0.,0.));
#3448=CARTESIAN_POINT('',(0.577350269189626,0.,0.));
#3449=CARTESIAN_POINT('',(0.577350269189626,0.,0.));
#3450=CARTESIAN_POINT('Origin',(0.288675134594813,0.,0.5));
#3451=CARTESIAN_POINT('',(0.288675134594813,0.,0.5));
#3452=CARTESIAN_POINT('',(0.288675134594813,0.,0.5));
#3453=CARTESIAN_POINT('',(0.288675134594813,0.,0.5));
#3454=CARTESIAN_POINT('Origin',(-0.288675134594813,0.,0.5));
#3455=CARTESIAN_POINT('',(-0.288675134594813,0.,0.5));
#3456=CARTESIAN_POINT('',(-0.288675134594813,0.,0.5));
#3457=CARTESIAN_POINT('',(-0.288675134594813,0.,0.5));
#3458=CARTESIAN_POINT('Origin',(-0.577350269189626,0.,-7.07050159149938E-17));
#3459=CARTESIAN_POINT('',(-0.577350269189626,0.,-7.07050159149938E-17));
#3460=CARTESIAN_POINT('',(-0.577350269189626,0.,-7.07050159149938E-17));
#3461=CARTESIAN_POINT('',(-0.577350269189626,0.,-7.07050159149938E-17));
#3462=CARTESIAN_POINT('Origin',(-0.288675134594813,0.,-0.5));
#3463=CARTESIAN_POINT('',(-0.288675134594813,0.,-0.5));
#3464=CARTESIAN_POINT('Origin',(0.,0.4,0.));
#3465=CARTESIAN_POINT('Origin',(0.,0.,0.));
#3757=UNCERTAINTY_MEASURE_WITH_UNIT(LENGTH_MEASURE(0.001),#3774,
'DISTANCE_ACCURACY_VALUE',
'Maximum model space distance between geometric entities at asserted c
onnectivities');
#3760=UNCERTAINTY_MEASURE_WITH_UNIT(LENGTH_MEASURE(0.001),#3774,
'DISTANCE_ACCURACY_VALUE',
'Maximum model space distance between geometric entities at asserted c
onnectivities');
#3770=(
GEOMETRIC_REPRESENTATION_CONTEXT(3)
GLOBAL_UNCERTAINTY_ASSIGNED_CONTEXT((#3757))
GLOBAL_UNIT_ASSIGNED_CONTEXT((#3774,#3776,#3777))
REPRESENTATION_CONTEXT('','3D')
);
#3773=(
GEOMETRIC_REPRESENTATION_CONTEXT(3)
GLOBAL_UNCERTAINTY_ASSIGNED_CONTEXT((#3760))
GLOBAL_UNIT_ASSIGNED_CONTEXT((#3774,#3776,#3777))
REPRESENTATION_CONTEXT('','3D')
);
#3774=(
LENGTH_UNIT()
NAMED_UNIT(*)
SI_UNIT(.CENTI.,.METRE.)
);
#3776=(
NAMED_UNIT(*)
PLANE_ANGLE_UNIT()
SI_UNIT($,.RADIAN.)
);
#3777=(
NAMED_UNIT(*)
SI_UNIT($,.STERADIAN.)
SOLID_ANGLE_UNIT()
);
#3787=SHAPE_DEFINITION_REPRESENTATION(#3802,#3822);
#3802=PRODUCT_DEFINITION_SHAPE('',$,#3835);
#3822=SHAPE_REPRESENTATION('',(#2426),#3770);
#3825=PRODUCT_DEFINITION_CONTEXT('part definition',#3863,'design');
#3835=PRODUCT_DEFINITION('Hex Bolt - M6 x 30 mm',
'Hex Bolt - M6 x 30 mm',#3847,#3825);
#3847=PRODUCT_DEFINITION_FORMATION('',$,#3874);
#3863=APPLICATION_CONTEXT(
'Core Data for Automotive Mechanical Design Process');
#3864=PRODUCT_CONTEXT('part definition',#3863,'mechanical');
#3874=PRODUCT('Hex Bolt - M6 x 30 mm','Hex Bolt - M6 x 30 mm',
'Hex Bolt - M6 x 30 mm',(#3864));
#3947=COLOUR_RGB('Black',0.12,0.14,0.17);
#3948=FILL_AREA_STYLE_COLOUR('',#3947);
#3949=FILL_AREA_STYLE('',(#3948));
#3950=SURFACE_STYLE_FILL_AREA(#3949);
#3951=SURFACE_SIDE_STYLE('',(#3950));
#3952=SURFACE_STYLE_USAGE(.BOTH.,#3951);
#3953=PRESENTATION_STYLE_ASSIGNMENT((#3952));
ENDSEC;
END-ISO-10303-21;
